ISO-10303-21;
HEADER;
/* Generated by software containing ST-Developer
 * from STEP Tools, Inc. (www.steptools.com) 
 */
/* OPTION: using custom renumber hook */

FILE_DESCRIPTION(
/* description */ ('STEP AP242 Edition 2', 'CAx-IF Rec.Pracs.---Representation and Presentation of Product Manufa
cturing Information (PMI)---4.0---2014-10-13', 'CAx-IF Rec.Pracs.---3D Tessellated Geometry---0.4---2014-09-14', '2;1', 'CAx-IF Rec.Pracs.---User Defined Attributes---1.5---2016-08-15'),
/* implementation_level */ '2;1');

FILE_NAME(
/* name */ 'Heavy hex bolt 3_8-16 x 1.5.step',
/* time_stamp */ '2026-10-07T00:00:55Z',
/* author */ (''),
/* organization */ (''),
/* preprocessor_version */ 'ST-DEVELOPER v20',
/* originating_system */ 'ONSHAPE BY PTC INC, 1.221',
/* authorisation */ '  ');

FILE_SCHEMA (('AP242_MANAGED_MODEL_BASED_3D_ENGINEERING_MIM_LF { 1 0 10303 442 3 1 4 }'));
ENDSEC;

DATA;
#117=SHAPE_REPRESENTATION_RELATIONSHIP('','',#4473,#128);
#128=ADVANCED_BREP_SHAPE_REPRESENTATION('',(#4449),#8536);
#139=TOROIDAL_SURFACE('',#4511,0.0055245,0.000762);
#193=CONICAL_SURFACE('',#4498,0.0087376,1.0471975511966);
#194=CONICAL_SURFACE('',#4500,0.0087376,1.0471975511966);
#195=CONICAL_SURFACE('',#4502,0.0087376,1.0471975511966);
#196=CONICAL_SURFACE('',#4504,0.0087376,1.0471975511966);
#197=CONICAL_SURFACE('',#4506,0.0087376,1.0471975511966);
#198=CONICAL_SURFACE('',#4508,0.0087376,1.0471975511966);
#199=CONICAL_SURFACE('',#4512,0.0039032404234375,0.785398163397448);
#204=CYLINDRICAL_SURFACE('',#4493,0.0047625);
#308=CIRCLE('',#4492,0.0055245);
#309=CIRCLE('',#4494,0.0047625);
#310=CIRCLE('',#4495,0.0047625);
#311=CIRCLE('',#4497,0.0039032404234375);
#312=CIRCLE('',#4499,0.0087376);
#313=CIRCLE('',#4501,0.0087376);
#314=CIRCLE('',#4503,0.0087376);
#315=CIRCLE('',#4505,0.0087376);
#316=CIRCLE('',#4507,0.0087376);
#317=CIRCLE('',#4509,0.0087376);
#583=B_SPLINE_CURVE_WITH_KNOTS('',3,(#6407,#6408,#6409,#6410),
 .UNSPECIFIED.,.F.,.F.,(4,4),(2.38073112704607E-7,0.00510460360858836),
 .UNSPECIFIED.);
#584=B_SPLINE_CURVE_WITH_KNOTS('',3,(#6412,#6413,#6414,#6415),
 .UNSPECIFIED.,.F.,.F.,(4,4),(0.00510460360858836,0.0101898849784681),
 .UNSPECIFIED.);
#585=B_SPLINE_CURVE_WITH_KNOTS('',3,(#6424,#6425,#6426,#6427),
 .UNSPECIFIED.,.F.,.F.,(4,4),(2.38073112713057E-7,0.00510460360858837),
 .UNSPECIFIED.);
#586=B_SPLINE_CURVE_WITH_KNOTS('',3,(#6429,#6430,#6431,#6432),
 .UNSPECIFIED.,.F.,.F.,(4,4),(0.00510460360858837,0.0101898849784681),
 .UNSPECIFIED.);
#587=B_SPLINE_CURVE_WITH_KNOTS('',3,(#6438,#6439,#6440,#6441),
 .UNSPECIFIED.,.F.,.F.,(4,4),(0.0141037246460291,0.0192101526638855),
 .UNSPECIFIED.);
#588=B_SPLINE_CURVE_WITH_KNOTS('',3,(#6443,#6444,#6445,#6446),
 .UNSPECIFIED.,.F.,.F.,(4,4),(0.00900032873565963,0.0141037246460291),
 .UNSPECIFIED.);
#589=B_SPLINE_CURVE_WITH_KNOTS('',3,(#6452,#6453,#6454,#6455),
 .UNSPECIFIED.,.F.,.F.,(4,4),(2.38073112724182E-7,0.00510460360858838),
 .UNSPECIFIED.);
#590=B_SPLINE_CURVE_WITH_KNOTS('',3,(#6457,#6458,#6459,#6460),
 .UNSPECIFIED.,.F.,.F.,(4,4),(0.00510460360858838,0.0101898849784681),
 .UNSPECIFIED.);
#591=B_SPLINE_CURVE_WITH_KNOTS('',3,(#6466,#6467,#6468,#6469),
 .UNSPECIFIED.,.F.,.F.,(4,4),(2.38073112713057E-7,0.00510460360858837),
 .UNSPECIFIED.);
#592=B_SPLINE_CURVE_WITH_KNOTS('',3,(#6471,#6472,#6473,#6474),
 .UNSPECIFIED.,.F.,.F.,(4,4),(0.00510460360858837,0.0101898849784681),
 .UNSPECIFIED.);
#593=B_SPLINE_CURVE_WITH_KNOTS('',3,(#6477,#6478,#6479,#6480),
 .UNSPECIFIED.,.F.,.F.,(4,4),(0.00900032873565963,0.0141037246460291),
 .UNSPECIFIED.);
#594=B_SPLINE_CURVE_WITH_KNOTS('',3,(#6482,#6483,#6484,#6485),
 .UNSPECIFIED.,.F.,.F.,(4,4),(0.0141037246460291,0.0192101526638855),
 .UNSPECIFIED.);
#699=ORIENTED_EDGE('',*,*,#1869,.F.);
#700=ORIENTED_EDGE('',*,*,#1870,.T.);
#701=ORIENTED_EDGE('',*,*,#1871,.T.);
#702=ORIENTED_EDGE('',*,*,#1872,.T.);
#703=ORIENTED_EDGE('',*,*,#1873,.F.);
#704=ORIENTED_EDGE('',*,*,#1874,.F.);
#705=ORIENTED_EDGE('',*,*,#1875,.T.);
#706=ORIENTED_EDGE('',*,*,#1876,.T.);
#707=ORIENTED_EDGE('',*,*,#1869,.T.);
#708=ORIENTED_EDGE('',*,*,#1877,.F.);
#709=ORIENTED_EDGE('',*,*,#1878,.F.);
#710=ORIENTED_EDGE('',*,*,#1879,.T.);
#711=ORIENTED_EDGE('',*,*,#1880,.T.);
#712=ORIENTED_EDGE('',*,*,#1874,.T.);
#713=ORIENTED_EDGE('',*,*,#1881,.F.);
#714=ORIENTED_EDGE('',*,*,#1882,.F.);
#715=ORIENTED_EDGE('',*,*,#1883,.T.);
#716=ORIENTED_EDGE('',*,*,#1884,.T.);
#717=ORIENTED_EDGE('',*,*,#1878,.T.);
#718=ORIENTED_EDGE('',*,*,#1885,.F.);
#719=ORIENTED_EDGE('',*,*,#1886,.F.);
#720=ORIENTED_EDGE('',*,*,#1887,.T.);
#721=ORIENTED_EDGE('',*,*,#1888,.T.);
#722=ORIENTED_EDGE('',*,*,#1882,.T.);
#723=ORIENTED_EDGE('',*,*,#1889,.F.);
#724=ORIENTED_EDGE('',*,*,#1872,.F.);
#725=ORIENTED_EDGE('',*,*,#1890,.T.);
#726=ORIENTED_EDGE('',*,*,#1891,.T.);
#727=ORIENTED_EDGE('',*,*,#1886,.T.);
#728=ORIENTED_EDGE('',*,*,#1892,.F.);
#729=ORIENTED_EDGE('',*,*,#1893,.T.);
#730=ORIENTED_EDGE('',*,*,#1873,.T.);
#731=ORIENTED_EDGE('',*,*,#1892,.T.);
#732=ORIENTED_EDGE('',*,*,#1889,.T.);
#733=ORIENTED_EDGE('',*,*,#1885,.T.);
#734=ORIENTED_EDGE('',*,*,#1881,.T.);
#735=ORIENTED_EDGE('',*,*,#1877,.T.);
#736=ORIENTED_EDGE('',*,*,#1894,.T.);
#737=ORIENTED_EDGE('',*,*,#1895,.T.);
#738=ORIENTED_EDGE('',*,*,#1896,.T.);
#739=ORIENTED_EDGE('',*,*,#1891,.F.);
#740=ORIENTED_EDGE('',*,*,#1897,.F.);
#741=ORIENTED_EDGE('',*,*,#1887,.F.);
#742=ORIENTED_EDGE('',*,*,#1898,.F.);
#743=ORIENTED_EDGE('',*,*,#1890,.F.);
#744=ORIENTED_EDGE('',*,*,#1871,.F.);
#745=ORIENTED_EDGE('',*,*,#1888,.F.);
#746=ORIENTED_EDGE('',*,*,#1899,.F.);
#747=ORIENTED_EDGE('',*,*,#1883,.F.);
#748=ORIENTED_EDGE('',*,*,#1884,.F.);
#749=ORIENTED_EDGE('',*,*,#1900,.F.);
#750=ORIENTED_EDGE('',*,*,#1879,.F.);
#751=ORIENTED_EDGE('',*,*,#1901,.F.);
#752=ORIENTED_EDGE('',*,*,#1875,.F.);
#753=ORIENTED_EDGE('',*,*,#1880,.F.);
#754=ORIENTED_EDGE('',*,*,#1902,.F.);
#755=ORIENTED_EDGE('',*,*,#1870,.F.);
#756=ORIENTED_EDGE('',*,*,#1876,.F.);
#757=ORIENTED_EDGE('',*,*,#1899,.T.);
#758=ORIENTED_EDGE('',*,*,#1897,.T.);
#759=ORIENTED_EDGE('',*,*,#1898,.T.);
#760=ORIENTED_EDGE('',*,*,#1902,.T.);
#761=ORIENTED_EDGE('',*,*,#1901,.T.);
#762=ORIENTED_EDGE('',*,*,#1900,.T.);
#763=ORIENTED_EDGE('',*,*,#1893,.F.);
#764=ORIENTED_EDGE('',*,*,#1895,.F.);
#765=ORIENTED_EDGE('',*,*,#1894,.F.);
#766=ORIENTED_EDGE('',*,*,#1896,.F.);
#1869=EDGE_CURVE('',#2454,#2455,#2834,.T.);
#1870=EDGE_CURVE('',#2454,#2456,#583,.T.);
#1871=EDGE_CURVE('',#2456,#2457,#584,.T.);
#1872=EDGE_CURVE('',#2457,#2458,#2835,.T.);
#1873=EDGE_CURVE('',#2455,#2458,#2836,.T.);
#1874=EDGE_CURVE('',#2459,#2460,#2837,.T.);
#1875=EDGE_CURVE('',#2459,#2461,#585,.T.);
#1876=EDGE_CURVE('',#2461,#2454,#586,.T.);
#1877=EDGE_CURVE('',#2460,#2455,#2838,.T.);
#1878=EDGE_CURVE('',#2462,#2463,#2839,.T.);
#1879=EDGE_CURVE('',#2462,#2464,#587,.F.);
#1880=EDGE_CURVE('',#2464,#2459,#588,.F.);
#1881=EDGE_CURVE('',#2463,#2460,#2840,.T.);
#1882=EDGE_CURVE('',#2465,#2466,#2841,.T.);
#1883=EDGE_CURVE('',#2465,#2467,#589,.T.);
#1884=EDGE_CURVE('',#2467,#2462,#590,.T.);
#1885=EDGE_CURVE('',#2466,#2463,#2842,.T.);
#1886=EDGE_CURVE('',#2468,#2469,#2843,.T.);
#1887=EDGE_CURVE('',#2468,#2470,#591,.T.);
#1888=EDGE_CURVE('',#2470,#2465,#592,.T.);
#1889=EDGE_CURVE('',#2469,#2466,#2844,.T.);
#1890=EDGE_CURVE('',#2457,#2471,#593,.T.);
#1891=EDGE_CURVE('',#2471,#2468,#594,.T.);
#1892=EDGE_CURVE('',#2458,#2469,#2845,.T.);
#1893=EDGE_CURVE('',#2472,#2472,#308,.T.);
#1894=EDGE_CURVE('',#2473,#2473,#309,.F.);
#1895=EDGE_CURVE('',#2474,#2474,#310,.F.);
#1896=EDGE_CURVE('',#2475,#2475,#311,.T.);
#1897=EDGE_CURVE('',#2470,#2471,#312,.T.);
#1898=EDGE_CURVE('',#2471,#2456,#313,.T.);
#1899=EDGE_CURVE('',#2467,#2470,#314,.T.);
#1900=EDGE_CURVE('',#2464,#2467,#315,.T.);
#1901=EDGE_CURVE('',#2461,#2464,#316,.T.);
#1902=EDGE_CURVE('',#2456,#2461,#317,.T.);
#2454=VERTEX_POINT('',#6405);
#2455=VERTEX_POINT('',#6406);
#2456=VERTEX_POINT('',#6411);
#2457=VERTEX_POINT('',#6416);
#2458=VERTEX_POINT('',#6418);
#2459=VERTEX_POINT('',#6422);
#2460=VERTEX_POINT('',#6423);
#2461=VERTEX_POINT('',#6428);
#2462=VERTEX_POINT('',#6436);
#2463=VERTEX_POINT('',#6437);
#2464=VERTEX_POINT('',#6442);
#2465=VERTEX_POINT('',#6450);
#2466=VERTEX_POINT('',#6451);
#2467=VERTEX_POINT('',#6456);
#2468=VERTEX_POINT('',#6464);
#2469=VERTEX_POINT('',#6465);
#2470=VERTEX_POINT('',#6470);
#2471=VERTEX_POINT('',#6481);
#2472=VERTEX_POINT('',#6489);
#2473=VERTEX_POINT('',#6492);
#2474=VERTEX_POINT('',#6494);
#2475=VERTEX_POINT('',#6497);
#2834=LINE('',#6404,#3012);
#2835=LINE('',#6417,#3013);
#2836=LINE('',#6419,#3014);
#2837=LINE('',#6421,#3015);
#2838=LINE('',#6433,#3016);
#2839=LINE('',#6435,#3017);
#2840=LINE('',#6447,#3018);
#2841=LINE('',#6449,#3019);
#2842=LINE('',#6461,#3020);
#2843=LINE('',#6463,#3021);
#2844=LINE('',#6475,#3022);
#2845=LINE('',#6486,#3023);
#3012=VECTOR('',#5068,1.);
#3013=VECTOR('',#5069,1.);
#3014=VECTOR('',#5070,1.);
#3015=VECTOR('',#5073,1.);
#3016=VECTOR('',#5074,1.);
#3017=VECTOR('',#5077,1.);
#3018=VECTOR('',#5078,1.);
#3019=VECTOR('',#5081,1.);
#3020=VECTOR('',#5082,1.);
#3021=VECTOR('',#5085,1.);
#3022=VECTOR('',#5086,1.);
#3023=VECTOR('',#5089,1.);
#3190=EDGE_LOOP('',(#699,#700,#701,#702,#703));
#3191=EDGE_LOOP('',(#704,#705,#706,#707,#708));
#3192=EDGE_LOOP('',(#709,#710,#711,#712,#713));
#3193=EDGE_LOOP('',(#714,#715,#716,#717,#718));
#3194=EDGE_LOOP('',(#719,#720,#721,#722,#723));
#3195=EDGE_LOOP('',(#724,#725,#726,#727,#728));
#3196=EDGE_LOOP('',(#729));
#3197=EDGE_LOOP('',(#730,#731,#732,#733,#734,#735));
#3198=EDGE_LOOP('',(#736));
#3199=EDGE_LOOP('',(#737));
#3200=EDGE_LOOP('',(#738));
#3201=EDGE_LOOP('',(#739,#740,#741));
#3202=EDGE_LOOP('',(#742,#743,#744));
#3203=EDGE_LOOP('',(#745,#746,#747));
#3204=EDGE_LOOP('',(#748,#749,#750));
#3205=EDGE_LOOP('',(#751,#752,#753));
#3206=EDGE_LOOP('',(#754,#755,#756));
#3207=EDGE_LOOP('',(#757,#758,#759,#760,#761,#762));
#3208=EDGE_LOOP('',(#763));
#3209=EDGE_LOOP('',(#764));
#3210=EDGE_LOOP('',(#765));
#3211=EDGE_LOOP('',(#766));
#3567=FACE_BOUND('',#3190,.T.);
#3568=FACE_BOUND('',#3191,.T.);
#3569=FACE_BOUND('',#3192,.T.);
#3570=FACE_BOUND('',#3193,.T.);
#3571=FACE_BOUND('',#3194,.T.);
#3572=FACE_BOUND('',#3195,.T.);
#3573=FACE_BOUND('',#3196,.T.);
#3574=FACE_BOUND('',#3197,.T.);
#3575=FACE_BOUND('',#3198,.T.);
#3576=FACE_BOUND('',#3199,.T.);
#3577=FACE_BOUND('',#3200,.T.);
#3578=FACE_BOUND('',#3201,.T.);
#3579=FACE_BOUND('',#3202,.T.);
#3580=FACE_BOUND('',#3203,.T.);
#3581=FACE_BOUND('',#3204,.T.);
#3582=FACE_BOUND('',#3205,.T.);
#3583=FACE_BOUND('',#3206,.T.);
#3584=FACE_BOUND('',#3207,.T.);
#3585=FACE_BOUND('',#3208,.T.);
#3586=FACE_BOUND('',#3209,.T.);
#3587=FACE_BOUND('',#3210,.T.);
#3588=FACE_BOUND('',#3211,.T.);
#3944=PLANE('',#4485);
#3945=PLANE('',#4486);
#3946=PLANE('',#4487);
#3947=PLANE('',#4488);
#3948=PLANE('',#4489);
#3949=PLANE('',#4490);
#3950=PLANE('',#4491);
#3951=PLANE('',#4496);
#3952=PLANE('',#4510);
#4036=ADVANCED_FACE('',(#3567),#3944,.T.);
#4037=ADVANCED_FACE('',(#3568),#3945,.T.);
#4038=ADVANCED_FACE('',(#3569),#3946,.T.);
#4039=ADVANCED_FACE('',(#3570),#3947,.T.);
#4040=ADVANCED_FACE('',(#3571),#3948,.T.);
#4041=ADVANCED_FACE('',(#3572),#3949,.T.);
#4042=ADVANCED_FACE('',(#3573,#3574),#3950,.F.);
#4043=ADVANCED_FACE('',(#3575,#3576),#204,.T.);
#4044=ADVANCED_FACE('',(#3577),#3951,.T.);
#4045=ADVANCED_FACE('',(#3578),#193,.T.);
#4046=ADVANCED_FACE('',(#3579),#194,.T.);
#4047=ADVANCED_FACE('',(#3580),#195,.T.);
#4048=ADVANCED_FACE('',(#3581),#196,.T.);
#4049=ADVANCED_FACE('',(#3582),#197,.T.);
#4050=ADVANCED_FACE('',(#3583),#198,.T.);
#4051=ADVANCED_FACE('',(#3584),#3952,.T.);
#4052=ADVANCED_FACE('',(#3585,#3586),#139,.F.);
#4053=ADVANCED_FACE('',(#3587,#3588),#199,.T.);
#4323=CLOSED_SHELL('',(#4036,#4037,#4038,#4039,#4040,#4041,#4042,#4043,
#4044,#4045,#4046,#4047,#4048,#4049,#4050,#4051,#4052,#4053));
#4334=STYLED_ITEM('',(#4345),#4449);
#4345=PRESENTATION_STYLE_ASSIGNMENT((#4361));
#4361=SURFACE_STYLE_USAGE(.BOTH.,#4377);
#4377=SURFACE_SIDE_STYLE('',(#4393));
#4393=SURFACE_STYLE_FILL_AREA(#4409);
#4409=FILL_AREA_STYLE('',(#4425));
#4425=FILL_AREA_STYLE_COLOUR('',#4441);
#4441=COLOUR_RGB('', 0.66274510, 0.83137255, 0.94901961);
#4449=MANIFOLD_SOLID_BREP('Heavy hex bolt 3/8-16 x 1.5',#4323);
#4461=SHAPE_DEFINITION_REPRESENTATION(#8563,#4473);
#4473=SHAPE_REPRESENTATION('Heavy hex bolt 3/8-16 x 1.5',(#4484),#8536);
#4484=AXIS2_PLACEMENT_3D('',#6402,#5064,#5065);
#4485=AXIS2_PLACEMENT_3D('',#6403,#5066,#5067);
#4486=AXIS2_PLACEMENT_3D('',#6420,#5071,#5072);
#4487=AXIS2_PLACEMENT_3D('',#6434,#5075,#5076);
#4488=AXIS2_PLACEMENT_3D('',#6448,#5079,#5080);
#4489=AXIS2_PLACEMENT_3D('',#6462,#5083,#5084);
#4490=AXIS2_PLACEMENT_3D('',#6476,#5087,#5088);
#4491=AXIS2_PLACEMENT_3D('',#6487,#5090,#5091);
#4492=AXIS2_PLACEMENT_3D('',#6488,#5092,#5093);
#4493=AXIS2_PLACEMENT_3D('',#6490,#5094,#5095);
#4494=AXIS2_PLACEMENT_3D('',#6491,#5096,#5097);
#4495=AXIS2_PLACEMENT_3D('',#6493,#5098,#5099);
#4496=AXIS2_PLACEMENT_3D('',#6495,#5100,#5101);
#4497=AXIS2_PLACEMENT_3D('',#6496,#5102,#5103);
#4498=AXIS2_PLACEMENT_3D('',#6498,#5104,#5105);
#4499=AXIS2_PLACEMENT_3D('',#6499,#5106,#5107);
#4500=AXIS2_PLACEMENT_3D('',#6500,#5108,#5109);
#4501=AXIS2_PLACEMENT_3D('',#6501,#5110,#5111);
#4502=AXIS2_PLACEMENT_3D('',#6502,#5112,#5113);
#4503=AXIS2_PLACEMENT_3D('',#6503,#5114,#5115);
#4504=AXIS2_PLACEMENT_3D('',#6504,#5116,#5117);
#4505=AXIS2_PLACEMENT_3D('',#6505,#5118,#5119);
#4506=AXIS2_PLACEMENT_3D('',#6506,#5120,#5121);
#4507=AXIS2_PLACEMENT_3D('',#6507,#5122,#5123);
#4508=AXIS2_PLACEMENT_3D('',#6508,#5124,#5125);
#4509=AXIS2_PLACEMENT_3D('',#6509,#5126,#5127);
#4510=AXIS2_PLACEMENT_3D('',#6510,#5128,#5129);
#4511=AXIS2_PLACEMENT_3D('',#6511,#5130,#5131);
#4512=AXIS2_PLACEMENT_3D('',#6512,#5132,#5133);
#5064=DIRECTION('',(0.,0.,1.));
#5065=DIRECTION('',(1.,0.,0.));
#5066=DIRECTION('',(-0.866025403784439,0.5,0.));
#5067=DIRECTION('',(-0.5,-0.866025403784439,0.));
#5068=DIRECTION('',(0.,0.,-1.));
#5069=DIRECTION('',(0.,0.,-1.));
#5070=DIRECTION('',(0.5,0.866025403784439,0.));
#5071=DIRECTION('',(-0.866025403784438,-0.5,0.));
#5072=DIRECTION('',(0.5,-0.866025403784439,0.));
#5073=DIRECTION('',(0.,0.,-1.));
#5074=DIRECTION('',(-0.5,0.866025403784439,0.));
#5075=DIRECTION('',(0.,-1.,0.));
#5076=DIRECTION('',(0.,0.,-1.));
#5077=DIRECTION('',(0.,0.,-1.));
#5078=DIRECTION('',(-1.,0.,0.));
#5079=DIRECTION('',(0.866025403784439,-0.5,0.));
#5080=DIRECTION('',(0.5,0.866025403784439,0.));
#5081=DIRECTION('',(0.,0.,-1.));
#5082=DIRECTION('',(-0.5,-0.866025403784439,0.));
#5083=DIRECTION('',(0.866025403784438,0.5,0.));
#5084=DIRECTION('',(-0.5,0.866025403784438,0.));
#5085=DIRECTION('',(0.,0.,-1.));
#5086=DIRECTION('',(0.5,-0.866025403784439,0.));
#5087=DIRECTION('',(0.,1.,0.));
#5088=DIRECTION('',(0.,0.,1.));
#5089=DIRECTION('',(1.,0.,0.));
#5090=DIRECTION('',(0.,0.,1.));
#5091=DIRECTION('',(1.,0.,0.));
#5092=DIRECTION('',(0.,0.,1.));
#5093=DIRECTION('',(1.,0.,0.));
#5094=DIRECTION('',(0.,0.,1.));
#5095=DIRECTION('',(1.,0.,0.));
#5096=DIRECTION('',(0.,0.,-1.));
#5097=DIRECTION('',(-1.,0.,0.));
#5098=DIRECTION('',(0.,0.,1.));
#5099=DIRECTION('',(1.,0.,0.));
#5100=DIRECTION('',(0.,0.,-1.));
#5101=DIRECTION('',(1.,0.,0.));
#5102=DIRECTION('',(0.,0.,-1.));
#5103=DIRECTION('',(-1.,0.,0.));
#5104=DIRECTION('',(0.,0.,-1.));
#5105=DIRECTION('',(-1.,0.,0.));
#5106=DIRECTION('',(0.,0.,1.));
#5107=DIRECTION('',(1.,0.,0.));
#5108=DIRECTION('',(0.,0.,-1.));
#5109=DIRECTION('',(-1.,0.,0.));
#5110=DIRECTION('',(0.,0.,1.));
#5111=DIRECTION('',(1.,0.,0.));
#5112=DIRECTION('',(0.,0.,-1.));
#5113=DIRECTION('',(-1.,0.,0.));
#5114=DIRECTION('',(0.,0.,1.));
#5115=DIRECTION('',(1.,0.,0.));
#5116=DIRECTION('',(0.,0.,-1.));
#5117=DIRECTION('',(-1.,0.,0.));
#5118=DIRECTION('',(0.,0.,1.));
#5119=DIRECTION('',(1.,0.,0.));
#5120=DIRECTION('',(0.,0.,-1.));
#5121=DIRECTION('',(-1.,0.,0.));
#5122=DIRECTION('',(0.,0.,1.));
#5123=DIRECTION('',(1.,0.,0.));
#5124=DIRECTION('',(0.,0.,-1.));
#5125=DIRECTION('',(-1.,0.,0.));
#5126=DIRECTION('',(0.,0.,1.));
#5127=DIRECTION('',(1.,0.,0.));
#5128=DIRECTION('',(0.,0.,1.));
#5129=DIRECTION('',(1.,0.,0.));
#5130=DIRECTION('',(0.,0.,1.));
#5131=DIRECTION('',(1.,0.,0.));
#5132=DIRECTION('',(0.,0.,1.));
#5133=DIRECTION('',(1.,0.,0.));
#6402=CARTESIAN_POINT('',(0.,0.,0.));
#6403=CARTESIAN_POINT('',(-0.00413398187534589,0.010314933354332,0.0068072));
#6404=CARTESIAN_POINT('',(-0.0100893114241425,5.20417042793042E-18,0.0068072));
#6405=CARTESIAN_POINT('',(-0.0100893114241425,-1.7347234759768E-18,0.00602678904540461));
#6406=CARTESIAN_POINT('',(-0.0100893114241425,5.20417042793042E-18,0.));
#6407=CARTESIAN_POINT('',(-0.0100893114241426,-4.9274984480842E-17,0.00602678904540501));
#6408=CARTESIAN_POINT('',(-0.00926407226496803,0.00142935615208567,0.00650324109610025));
#6409=CARTESIAN_POINT('',(-0.00842644381484264,0.00288017118556803,0.00680720000000001));
#6410=CARTESIAN_POINT('',(-0.00756698356810691,0.0043688,0.00680720000000001));
#6411=CARTESIAN_POINT('',(-0.00756698356810691,0.0043688,0.0068072));
#6412=CARTESIAN_POINT('',(-0.00756698356810691,0.0043688,0.00680720000000001));
#6413=CARTESIAN_POINT('',(-0.00671073666523493,0.00585186313959776,0.00680720000000001));
#6414=CARTESIAN_POINT('',(-0.00586783431762229,0.00731181283148194,0.00650205143491084));
#6415=CARTESIAN_POINT('',(-0.00504465571207126,0.00873760000000003,0.00602678904540481));
#6416=CARTESIAN_POINT('',(-0.00504465571207127,0.0087376,0.00602678904540461));
#6417=CARTESIAN_POINT('',(-0.00504465571207127,0.0087376,0.0068072));
#6418=CARTESIAN_POINT('',(-0.00504465571207127,0.0087376,0.));
#6419=CARTESIAN_POINT('',(-0.00413398187534589,0.010314933354332,0.));
#6420=CARTESIAN_POINT('',(-0.00413398187534589,-0.010314933354332,0.0068072));
#6421=CARTESIAN_POINT('',(-0.00504465571207127,-0.0087376,0.0068072));
#6422=CARTESIAN_POINT('',(-0.00504465571207127,-0.0087376,0.00602678904540461));
#6423=CARTESIAN_POINT('',(-0.00504465571207127,-0.0087376,0.));
#6424=CARTESIAN_POINT('',(-0.00504465571207124,-0.00873760000000005,0.00602678904540501));
#6425=CARTESIAN_POINT('',(-0.00586989487124578,-0.00730824384791432,0.00650324109610026));
#6426=CARTESIAN_POINT('',(-0.00670752332137117,-0.00585742881443197,0.00680720000000001));
#6427=CARTESIAN_POINT('',(-0.0075669835681069,-0.0043688,0.00680720000000001));
#6428=CARTESIAN_POINT('',(-0.00756698356810691,-0.0043688,0.0068072));
#6429=CARTESIAN_POINT('',(-0.00756698356810691,-0.0043688,0.00680720000000001));
#6430=CARTESIAN_POINT('',(-0.00842323047097888,-0.00288573686040224,0.00680720000000001));
#6431=CARTESIAN_POINT('',(-0.00926613281859153,-0.00142578716851806,0.00650205143491085));
#6432=CARTESIAN_POINT('',(-0.0100893114241426,2.64498759817976E-17,0.00602678904540481));
#6433=CARTESIAN_POINT('',(-0.00413398187534589,-0.010314933354332,0.));
#6434=CARTESIAN_POINT('',(5.61756925238316E-18,-0.0087376,0.0068072));
#6435=CARTESIAN_POINT('',(0.00504465571207128,-0.0087376,0.0068072));
#6436=CARTESIAN_POINT('',(0.00504465571207127,-0.0087376,0.00602678904540461));
#6437=CARTESIAN_POINT('',(0.00504465571207128,-0.0087376,0.));
#6438=CARTESIAN_POINT('',(-2.36129909705544E-19,-0.0087376,0.0068072));
#6439=CARTESIAN_POINT('',(0.00170594066282747,-0.0087376,0.0068072));
#6440=CARTESIAN_POINT('',(0.00341327030332511,-0.0087376,0.00649772944785042));
#6441=CARTESIAN_POINT('',(0.00504465571207127,-0.0087376,0.00602678904540461));
#6442=CARTESIAN_POINT('',(0.,-0.0087376,0.0068072));
#6443=CARTESIAN_POINT('',(-0.00504465571207128,-0.0087376,0.00602678904540464));
#6444=CARTESIAN_POINT('',(-0.00340371094881485,-0.0087376,0.00650048899580034));
#6445=CARTESIAN_POINT('',(-0.0017049277051518,-0.0087376,0.0068072));
#6446=CARTESIAN_POINT('',(1.49859356627126E-18,-0.0087376,0.0068072));
#6447=CARTESIAN_POINT('',(5.61756925238316E-18,-0.0087376,0.));
#6448=CARTESIAN_POINT('',(0.00413398187534589,-0.010314933354332,0.0068072));
#6449=CARTESIAN_POINT('',(0.0100893114241425,3.46944695195361E-18,0.0068072));
#6450=CARTESIAN_POINT('',(0.0100893114241425,0.,0.00602678904540461));
#6451=CARTESIAN_POINT('',(0.0100893114241425,3.46944695195361E-18,0.));
#6452=CARTESIAN_POINT('',(0.0100893114241426,4.73615312627302E-17,0.00602678904540501));
#6453=CARTESIAN_POINT('',(0.00926407226496803,-0.00142935615208568,0.00650324109610025));
#6454=CARTESIAN_POINT('',(0.00842644381484264,-0.00288017118556803,0.00680720000000001));
#6455=CARTESIAN_POINT('',(0.00756698356810691,-0.0043688,0.00680720000000001));
#6456=CARTESIAN_POINT('',(0.00756698356810691,-0.0043688,0.0068072));
#6457=CARTESIAN_POINT('',(0.00756698356810691,-0.0043688,0.00680720000000001));
#6458=CARTESIAN_POINT('',(0.00671073666523493,-0.00585186313959775,0.00680720000000001));
#6459=CARTESIAN_POINT('',(0.00586783431762229,-0.00731181283148194,0.00650205143491084));
#6460=CARTESIAN_POINT('',(0.00504465571207126,-0.00873760000000003,0.00602678904540481));
#6461=CARTESIAN_POINT('',(0.00413398187534589,-0.010314933354332,0.));
#6462=CARTESIAN_POINT('',(0.0109999852608679,-0.00157733335433204,0.0068072));
#6463=CARTESIAN_POINT('',(0.00504465571207127,0.0087376,0.0068072));
#6464=CARTESIAN_POINT('',(0.00504465571207127,0.0087376,0.00602678904540461));
#6465=CARTESIAN_POINT('',(0.00504465571207127,0.0087376,0.));
#6466=CARTESIAN_POINT('',(0.00504465571207124,0.00873760000000004,0.00602678904540501));
#6467=CARTESIAN_POINT('',(0.00586989487124578,0.00730824384791432,0.00650324109610026));
#6468=CARTESIAN_POINT('',(0.00670752332137117,0.00585742881443197,0.00680720000000001));
#6469=CARTESIAN_POINT('',(0.0075669835681069,0.0043688,0.00680720000000001));
#6470=CARTESIAN_POINT('',(0.00756698356810691,0.0043688,0.0068072));
#6471=CARTESIAN_POINT('',(0.0075669835681069,0.0043688,0.00680720000000001));
#6472=CARTESIAN_POINT('',(0.00842323047097888,0.00288573686040224,0.00680720000000001));
#6473=CARTESIAN_POINT('',(0.00926613281859152,0.00142578716851806,0.00650205143491085));
#6474=CARTESIAN_POINT('',(0.0100893114241426,-2.79818636934923E-17,0.00602678904540481));
#6475=CARTESIAN_POINT('',(0.0109999852608679,-0.00157733335433204,0.));
#6476=CARTESIAN_POINT('',(0.,0.0087376,0.0068072));
#6477=CARTESIAN_POINT('',(-0.00504465571207128,0.0087376,0.00602678904540464));
#6478=CARTESIAN_POINT('',(-0.00340371094881485,0.0087376,0.00650048899580034));
#6479=CARTESIAN_POINT('',(-0.0017049277051518,0.0087376,0.0068072));
#6480=CARTESIAN_POINT('',(1.5036505349461E-18,0.0087376,0.0068072));
#6481=CARTESIAN_POINT('',(0.,0.0087376,0.0068072));
#6482=CARTESIAN_POINT('',(-2.3107294103071E-19,0.0087376,0.0068072));
#6483=CARTESIAN_POINT('',(0.00170594066282747,0.0087376,0.0068072));
#6484=CARTESIAN_POINT('',(0.00341327030332511,0.0087376,0.00649772944785042));
#6485=CARTESIAN_POINT('',(0.00504465571207127,0.0087376,0.00602678904540461));
#6486=CARTESIAN_POINT('',(0.,0.0087376,0.));
#6487=CARTESIAN_POINT('',(0.,0.,0.));
#6488=CARTESIAN_POINT('',(0.,0.,0.));
#6489=CARTESIAN_POINT('',(0.0055245,0.,0.));
#6490=CARTESIAN_POINT('',(0.,0.,-0.0381));
#6491=CARTESIAN_POINT('',(0.,0.,-0.0372407404234375));
#6492=CARTESIAN_POINT('',(-0.0047625,0.,-0.0372407404234375));
#6493=CARTESIAN_POINT('',(0.,0.,-0.000762));
#6494=CARTESIAN_POINT('',(0.0047625,0.,-0.000762));
#6495=CARTESIAN_POINT('',(-1.7347234759768E-18,0.,-0.0381));
#6496=CARTESIAN_POINT('',(0.,0.,-0.0381));
#6497=CARTESIAN_POINT('',(-0.0039032404234375,0.,-0.0381));
#6498=CARTESIAN_POINT('',(0.,0.,0.0068072));
#6499=CARTESIAN_POINT('',(0.,0.,0.0068072));
#6500=CARTESIAN_POINT('',(0.,0.,0.0068072));
#6501=CARTESIAN_POINT('',(0.,0.,0.0068072));
#6502=CARTESIAN_POINT('',(0.,0.,0.0068072));
#6503=CARTESIAN_POINT('',(0.,0.,0.0068072));
#6504=CARTESIAN_POINT('',(0.,0.,0.0068072));
#6505=CARTESIAN_POINT('',(0.,0.,0.0068072));
#6506=CARTESIAN_POINT('',(0.,0.,0.0068072));
#6507=CARTESIAN_POINT('',(0.,0.,0.0068072));
#6508=CARTESIAN_POINT('',(0.,0.,0.0068072));
#6509=CARTESIAN_POINT('',(0.,0.,0.0068072));
#6510=CARTESIAN_POINT('',(0.,0.,0.0068072));
#6511=CARTESIAN_POINT('',(0.,0.,-0.000762));
#6512=CARTESIAN_POINT('',(0.,0.,-0.0381));
#8534=MECHANICAL_DESIGN_GEOMETRIC_PRESENTATION_REPRESENTATION('',(#4334),#8535);
#8535=(
GEOMETRIC_REPRESENTATION_CONTEXT(3)
GLOBAL_UNCERTAINTY_ASSIGNED_CONTEXT((#8547))
GLOBAL_UNIT_ASSIGNED_CONTEXT((#8561,#8560,#8559))
REPRESENTATION_CONTEXT('MAS-680','TOP_LEVEL_ASSEMBLY_PART')
);
#8536=(
GEOMETRIC_REPRESENTATION_CONTEXT(3)
GLOBAL_UNCERTAINTY_ASSIGNED_CONTEXT((#8548))
GLOBAL_UNIT_ASSIGNED_CONTEXT((#8561,#8560,#8559))
REPRESENTATION_CONTEXT('Heavy hex bolt 3/8-16 x 1.5','COMPONENT_PART')
);
#8547=UNCERTAINTY_MEASURE_WITH_UNIT(LENGTH_MEASURE(1.E-8),#8561,
'DISTANCE_ACCURACY_VALUE','Maximum Tolerance applied to model');
#8548=UNCERTAINTY_MEASURE_WITH_UNIT(LENGTH_MEASURE(2.E-5),#8561,
'DISTANCE_ACCURACY_VALUE','Maximum Tolerance applied to model');
#8559=(
NAMED_UNIT(*)
SI_UNIT($,.STERADIAN.)
SOLID_ANGLE_UNIT()
);
#8560=(
NAMED_UNIT(*)
PLANE_ANGLE_UNIT()
SI_UNIT($,.RADIAN.)
);
#8561=(
LENGTH_UNIT()
NAMED_UNIT(*)
SI_UNIT($,.METRE.)
);
#8563=PRODUCT_DEFINITION_SHAPE('','',#8590);
#8590=PRODUCT_DEFINITION('','',#8614,#8602);
#8602=PRODUCT_DEFINITION_CONTEXT('',#8674,'design');
#8614=PRODUCT_DEFINITION_FORMATION_WITH_SPECIFIED_SOURCE('','',#8638,
 .NOT_KNOWN.);
#8638=PRODUCT('Heavy hex bolt 3/8-16 x 1.5',
'Heavy hex bolt 3/8-16 x 1.5','Heavy hex bolt 3/8-16 x 1.5',(#8662));
#8662=PRODUCT_CONTEXT('',#8674,'mechanical');
#8674=APPLICATION_CONTEXT('managed model based 3d engineering');
ENDSEC;
END-ISO-10303-21;
